ISO-10303-21;
HEADER;
FILE_DESCRIPTION (('STEP AP214'),
    '1' );
FILE_NAME ('Ball Seat Ring.step',
    '2026-10-09T13:48:35',
    ( '' ),
    ( '' ),
    'SwSTEP 2.0',
    'SolidWorks 2026',
    '' );
FILE_SCHEMA (( 'AUTOMOTIVE_DESIGN' ));
ENDSEC;

DATA;
#20=ORIENTED_EDGE ( 'NONE', *, *, #12798, .T. ) ;
#33=ORIENTED_EDGE ( 'NONE', *, *, #678, .T. ) ;
#66=EDGE_CURVE ( 'NONE', #3183, #7147, #11899, .T. ) ;
#79=EDGE_CURVE ( 'NONE', #8805, #20876, #2608, .T. ) ;
#103=EDGE_LOOP ( 'NONE', ( #22830, #9902, #9803, #18093 ) ) ;
#116=PRODUCT_DEFINITION ( 'UNKNOWN', '', #15975, #23669 ) ;
#143=EDGE_CURVE ( 'NONE', #568, #7147, #7639, .T. ) ;
#222=DIRECTION ( 'NONE',  ( -1.000000000000000000, 0.000000000000000000, 0.000000000000000000 ) ) ;
#225=FACE_OUTER_BOUND ( 'NONE', #6977, .T. ) ;
#237=ADVANCED_FACE ( 'NONE', ( #3364 ), #23073, .T. ) ;
#240=TOROIDAL_SURFACE ( 'NONE', #10710, 7.200000000000000178, 0.1000000000000000056 ) ;
#303=ADVANCED_FACE ( 'NONE', ( #21762 ), #7109, .T. ) ;
#323=DIRECTION ( 'NONE',  ( 0.000000000000000000, -5.996565258237000474E-10, 1.000000000000000000 ) ) ;
#343=FACE_OUTER_BOUND ( 'NONE', #17510, .T. ) ;
#352=ORIENTED_EDGE ( 'NONE', *, *, #7893, .F. ) ;
#370=DIRECTION ( 'NONE',  ( -1.000000000000000000, 0.000000000000000000, 1.562509794170000285E-11 ) ) ;
#374=CIRCLE ( 'NONE', #16631, 0.1000000000000004635 ) ;
#455=ORIENTED_EDGE ( 'NONE', *, *, #4994, .F. ) ;
#489=CARTESIAN_POINT ( 'NONE',  ( -8.000000000000000000, 9.651424765286998664, 0.000000000000000000 ) ) ;
#525=DIRECTION ( 'NONE',  ( 0.000000000000000000, -0.9998947838056817528, -0.01450590632083973396 ) ) ;
#568=VERTEX_POINT ( 'NONE', #9622 ) ;
#595=( NAMED_UNIT ( * ) SI_UNIT ( $, .STERADIAN. ) SOLID_ANGLE_UNIT ( ) );
#622=AXIS2_PLACEMENT_3D ( 'NONE', #21561, #12361, #8721 ) ;
#674=ADVANCED_BREP_SHAPE_REPRESENTATION ( '', ( #9053, #4390 ), #20254 ) ;
#678=EDGE_CURVE ( 'NONE', #20171, #3348, #9524, .T. ) ;
#716=ORIENTED_EDGE ( 'NONE', *, *, #17809, .F. ) ;
#767=ORIENTED_EDGE ( 'NONE', *, *, #4237, .F. ) ;
#811=CARTESIAN_POINT ( 'NONE',  ( -10.90000000000000036, -7.200000000000000178, -4.317526974828999792E-09 ) ) ;
#821=ADVANCED_FACE ( 'NONE', ( #4665 ), #14975, .T. ) ;
#831=VECTOR ( 'NONE', #22809, 1000.000000000000000 ) ;
#995=DIRECTION ( 'NONE',  ( 0.000000000000000000, -0.9998172265789604385, -0.01911840568550923769 ) ) ;
#1071=CARTESIAN_POINT ( 'NONE',  ( -8.000000000000000000, 10.50000000000000000, 0.000000000000000000 ) ) ;
#1147=DIRECTION ( 'NONE',  ( 0.000000000000000000, -0.9997423213046380264, -0.02270002185933085032 ) ) ;
#1155=AXIS2_PLACEMENT_3D ( 'NONE', #18085, #10820, #995 ) ;
#1266=EDGE_LOOP ( 'NONE', ( #12701, #18089 ) ) ;
#1424=CIRCLE ( 'NONE', #7199, 9.651424765286998664 ) ;
#1425=CIRCLE ( 'NONE', #622, 12.50000000000000533 ) ;
#1435=FACE_OUTER_BOUND ( 'NONE', #2398, .T. ) ;
#1465=AXIS2_PLACEMENT_3D ( 'NONE', #15450, #22836, #22601 ) ;
#1499=EDGE_LOOP ( 'NONE', ( #18224, #22941 ) ) ;
#1509=AXIS2_PLACEMENT_3D ( 'NONE', #15833, #17544, #15703 ) ;
#1641=DIRECTION ( 'NONE',  ( 0.000000000000000000, -1.000000000000000000, 0.000000000000000000 ) ) ;
#1677=UNCERTAINTY_MEASURE_WITH_UNIT (LENGTH_MEASURE( 1.000000000000000082E-05 ), #20239, 'distance_accuracy_value', 'NONE');
#1704=SHAPE_REPRESENTATION_RELATIONSHIP ( 'NONE' , 'NONE' ,  #14475, #674 ) ;
#1721=SURFACE_STYLE_USAGE ( .BOTH. , #18318 ) ;
#1728=ORIENTED_EDGE ( 'NONE', *, *, #8958, .F. ) ;
#1755=FACE_OUTER_BOUND ( 'NONE', #103, .T. ) ;
#1761=VERTEX_POINT ( 'NONE', #21434 ) ;
#1803=FACE_OUTER_BOUND ( 'NONE', #1499, .T. ) ;
#1822=PLANE ( 'NONE',  #14581 ) ;
#1829=ORIENTED_EDGE ( 'NONE', *, *, #143, .F. ) ;
#1868=AXIS2_PLACEMENT_3D ( 'NONE', #9397, #17932, #6901 ) ;
#1893=DIRECTION ( 'NONE',  ( 0.000000000000000000, -0.9998843904358519774, -0.01520545174352925036 ) ) ;
#1957=( LENGTH_UNIT ( ) NAMED_UNIT ( * ) SI_UNIT ( .MILLI., .METRE. ) );
#1959=ORIENTED_EDGE ( 'NONE', *, *, #8542, .F. ) ;
#1992=EDGE_CURVE ( 'NONE', #8805, #1761, #374, .T. ) ;
#2151=CIRCLE ( 'NONE', #15677, 7.200000000000000178 ) ;
#2248=CIRCLE ( 'NONE', #18503, 10.59999999999999964 ) ;
#2398=EDGE_LOOP ( 'NONE', ( #12358, #4368, #19153, #3844 ) ) ;
#2497=DIRECTION ( 'NONE',  ( 0.000000000000000000, 1.000000000000000000, 0.000000000000000000 ) ) ;
#2546=ORIENTED_EDGE ( 'NONE', *, *, #19568, .F. ) ;
#2547=CIRCLE ( 'NONE', #18800, 7.100000000000000533 ) ;
#2548=CYLINDRICAL_SURFACE ( 'NONE', #14997, 7.100000000000000533 ) ;
#2582=DIRECTION ( 'NONE',  ( 1.000000000000000000, 0.000000000000000000, -2.088598344706999779E-09 ) ) ;
#2608=CIRCLE ( 'NONE', #1465, 7.142857142857000241 ) ;
#2619=AXIS2_PLACEMENT_3D ( 'NONE', #12169, #23045, #1147 ) ;
#2704=DIRECTION ( 'NONE',  ( -1.000000000000000000, 0.000000000000000000, 0.000000000000000000 ) ) ;
#2783=CARTESIAN_POINT ( 'NONE',  ( -8.000000000000000000, 1.322618543078999814E-14, 0.000000000000000000 ) ) ;
#2910=CARTESIAN_POINT ( 'NONE',  ( -10.90000000000000036, 1.358133300253999998E-14, 0.000000000000000000 ) ) ;
#2912=DIRECTION ( 'NONE',  ( 0.000000000000000000, -1.000000000000000000, 0.000000000000000000 ) ) ;
#2973=CIRCLE ( 'NONE', #18070, 0.09999999999999942268 ) ;
#2996=AXIS2_PLACEMENT_3D ( 'NONE', #7622, #14764, #20350 ) ;
#2997=DIRECTION ( 'NONE',  ( -1.000000000000000000, 0.000000000000000000, 0.000000000000000000 ) ) ;
#3015=ADVANCED_FACE ( 'NONE', ( #20471, #22272 ), #1822, .F. ) ;
#3131=ADVANCED_FACE ( 'NONE', ( #225 ), #16586, .F. ) ;
#3146=CARTESIAN_POINT ( 'NONE',  ( -8.099999999999999645, 1.323843189878000027E-14, 0.000000000000000000 ) ) ;
#3170=ADVANCED_FACE ( 'NONE', ( #343 ), #18530, .F. ) ;
#3183=VERTEX_POINT ( 'NONE', #23100 ) ;
#3229=EDGE_LOOP ( 'NONE', ( #20, #19235, #2546, #18356 ) ) ;
#3241=CARTESIAN_POINT ( 'NONE',  ( 0.5500000000000000444, 1.217911241751999838E-14, 0.000000000000000000 ) ) ;
#3242=ORIENTED_EDGE ( 'NONE', *, *, #20373, .F. ) ;
#3291=DIRECTION ( 'NONE',  ( 0.000000000000000000, -1.000000000000000000, -5.996561511235021317E-10 ) ) ;
#3327=DIRECTION ( 'NONE',  ( 0.000000000000000000, 0.000000000000000000, 1.000000000000000000 ) ) ;
#3348=VERTEX_POINT ( 'NONE', #1071 ) ;
#3364=FACE_OUTER_BOUND ( 'NONE', #5541, .T. ) ;
#3462=TOROIDAL_SURFACE ( 'NONE', #4609, 10.50000000000000000, 0.1000000000000000056 ) ;
#3467=DIRECTION ( 'NONE',  ( 0.8206518289197729521, -0.5714285394435874021, -4.207939614820930173E-10 ) ) ;
#3548=FILL_AREA_STYLE ('',( #20140 ) ) ;
#3598=DIRECTION ( 'NONE',  ( -1.000000000000000000, 0.000000000000000000, 0.000000000000000000 ) ) ;
#3682=AXIS2_PLACEMENT_3D ( 'NONE', #18630, #7599, #7130 ) ;
#3758=DIRECTION ( 'NONE',  ( 1.000000000000000000, 0.000000000000000000, 0.000000000000000000 ) ) ;
#3844=ORIENTED_EDGE ( 'NONE', *, *, #20912, .F. ) ;
#3966=CARTESIAN_POINT ( 'NONE',  ( -10.90000000000000036, -7.100000000000000533, 0.000000000000000000 ) ) ;
#4103=ORIENTED_EDGE ( 'NONE', *, *, #15455, .F. ) ;
#4109=CARTESIAN_POINT ( 'NONE',  ( -8.000000000000000000, 1.322618543078999814E-14, 0.000000000000000000 ) ) ;
#4194=ORIENTED_EDGE ( 'NONE', *, *, #13685, .T. ) ;
#4237=EDGE_CURVE ( 'NONE', #15884, #16101, #8813, .T. ) ;
#4261=LINE ( 'NONE', #22183, #15440 ) ;
#4368=ORIENTED_EDGE ( 'NONE', *, *, #4237, .T. ) ;
#4390=AXIS2_PLACEMENT_3D ( 'NONE', #8983, #23856, #3758 ) ;
#4540=DIRECTION ( 'NONE',  ( -1.000000000000000000, 0.000000000000000000, -1.562512024529000220E-11 ) ) ;
#4609=AXIS2_PLACEMENT_3D ( 'NONE', #18480, #16537, #1893 ) ;
#4665=FACE_OUTER_BOUND ( 'NONE', #8234, .T. ) ;
#4841=MECHANICAL_DESIGN_GEOMETRIC_PRESENTATION_REPRESENTATION('',(#19537),#22224);
#4881=CARTESIAN_POINT ( 'NONE',  ( -8.099999999999999645, -10.59999999999999964, 0.000000000000000000 ) ) ;
#4936=DIRECTION ( 'NONE',  ( 0.000000000000000000, 0.9998947838056817528, 0.01450590632083973396 ) ) ;
#4956=DIRECTION ( 'NONE',  ( -1.000000000000000000, 0.000000000000000000, 0.000000000000000000 ) ) ;
#4994=EDGE_CURVE ( 'NONE', #7168, #15263, #15422, .T. ) ;
#5025=EDGE_LOOP ( 'NONE', ( #14679, #19825 ) ) ;
#5175=DIRECTION ( 'NONE',  ( -1.000000000000000000, 4.163336342344362068E-12, 0.000000000000000000 ) ) ;
#5203=DIRECTION ( 'NONE',  ( -1.000000000000000000, 0.000000000000000000, 0.000000000000000000 ) ) ;
#5276=ORIENTED_EDGE ( 'NONE', *, *, #17809, .T. ) ;
#5336=DIRECTION ( 'NONE',  ( 0.000000000000000000, -1.000000000000000000, 0.000000000000000000 ) ) ;
#5368=CARTESIAN_POINT ( 'NONE',  ( 0.000000000000000000, 2.449293598294999890E-14, 0.000000000000000000 ) ) ;
#5541=EDGE_LOOP ( 'NONE', ( #17408, #12788, #16808, #10611 ) ) ;
#5715=CARTESIAN_POINT ( 'NONE',  ( -8.035714285714000482, 1.323055916935999825E-14, 0.000000000000000000 ) ) ;
#5892=DIRECTION ( 'NONE',  ( 0.000000000000000000, 1.000000000000000000, 0.000000000000000000 ) ) ;
#5935=ORIENTED_EDGE ( 'NONE', *, *, #13685, .F. ) ;
#5970=ADVANCED_FACE ( 'NONE', ( #14202 ), #20873, .T. ) ;
#6250=VERTEX_POINT ( 'NONE', #16801 ) ;
#6271=ORIENTED_EDGE ( 'NONE', *, *, #22945, .F. ) ;
#6312=ORIENTED_EDGE ( 'NONE', *, *, #20620, .T. ) ;
#6374=CIRCLE ( 'NONE', #21076, 10.50000000000000000 ) ;
#6508=AXIS2_PLACEMENT_3D ( 'NONE', #6787, #18403, #3291 ) ;
#6529=DIRECTION ( 'NONE',  ( 0.000000000000000000, -1.000000000000000000, 0.000000000000000000 ) ) ;
#6607=EDGE_LOOP ( 'NONE', ( #455, #7646, #6312, #6271 ) ) ;
#6705=ORIENTED_EDGE ( 'NONE', *, *, #66, .T. ) ;
#6733=ORIENTED_EDGE ( 'NONE', *, *, #12772, .F. ) ;
#6787=CARTESIAN_POINT ( 'NONE',  ( -10.90000000000000036, 7.200000000000000178, 4.317524282537999640E-09 ) ) ;
#6792=AXIS2_PLACEMENT_3D ( 'NONE', #20804, #7965, #17286 ) ;
#6826=CIRCLE ( 'NONE', #18063, 0.09999999999999939493 ) ;
#6853=CIRCLE ( 'NONE', #20787, 9.574826156038998448 ) ;
#6855=PRODUCT_CONTEXT ( 'NONE', #8034, 'mechanical' ) ;
#6885=ADVANCED_FACE ( 'NONE', ( #15945 ), #17794, .F. ) ;
#6901=DIRECTION ( 'NONE',  ( 0.000000000000000000, -1.000000000000000000, 0.000000000000000000 ) ) ;
#6912=DIRECTION ( 'NONE',  ( 0.000000000000000000, 1.792956356299999973E-10, -1.000000000000000000 ) ) ;
#6968=CARTESIAN_POINT ( 'NONE',  ( -10.34021276376999943, 7.200000000000000178, 5.302004252305999846E-09 ) ) ;
#6977=EDGE_LOOP ( 'NONE', ( #18583, #5276, #19226, #767 ) ) ;
#7098=EDGE_CURVE ( 'NONE', #6250, #3183, #19187, .T. ) ;
#7109=TOROIDAL_SURFACE ( 'NONE', #10210, 10.50000000000000000, 0.1000000000000000056 ) ;
#7130=DIRECTION ( 'NONE',  ( 0.000000000000000000, 0.000000000000000000, 1.000000000000000000 ) ) ;
#7147=VERTEX_POINT ( 'NONE', #12535 ) ;
#7168=VERTEX_POINT ( 'NONE', #12297 ) ;
#7199=AXIS2_PLACEMENT_3D ( 'NONE', #7652, #22421, #18672 ) ;
#7384=( NAMED_UNIT ( * ) PLANE_ANGLE_UNIT ( ) SI_UNIT ( $, .RADIAN. ) );
#7399=CARTESIAN_POINT ( 'NONE',  ( -11.00000000000000000, 1.359357947053999856E-14, 0.000000000000000000 ) ) ;
#7436=ORIENTED_EDGE ( 'NONE', *, *, #20620, .F. ) ;
#7484=CARTESIAN_POINT ( 'NONE',  ( -8.000000000000000000, -10.50000000000000000, 0.000000000000000000 ) ) ;
#7505=VERTEX_POINT ( 'NONE', #4881 ) ;
#7599=DIRECTION ( 'NONE',  ( -1.000000000000000000, 0.000000000000000000, 0.000000000000000000 ) ) ;
#7602=ORIENTED_EDGE ( 'NONE', *, *, #8754, .T. ) ;
#7611=ORIENTED_EDGE ( 'NONE', *, *, #13076, .F. ) ;
#7622=CARTESIAN_POINT ( 'NONE',  ( 0.000000000000000000, 1.224646799146999965E-14, 0.000000000000000000 ) ) ;
#7639=CIRCLE ( 'NONE', #16135, 0.09999999999999939493 ) ;
#7646=ORIENTED_EDGE ( 'NONE', *, *, #9697, .T. ) ;
#7652=CARTESIAN_POINT ( 'NONE',  ( -8.000000000000000000, 1.322618543078999814E-14, 0.000000000000000000 ) ) ;
#7728=DIRECTION ( 'NONE',  ( 0.000000000000000000, 1.000000000000000000, 5.996565258237018052E-10 ) ) ;
#7730=EDGE_CURVE ( 'NONE', #7738, #16445, #22666, .T. ) ;
#7738=VERTEX_POINT ( 'NONE', #19503 ) ;
#7768=CARTESIAN_POINT ( 'NONE',  ( -10.25814758309999952, 7.142857142857000241, 0.000000000000000000 ) ) ;
#7771=DIRECTION ( 'NONE',  ( 0.000000000000000000, -1.000000000000000000, 0.000000000000000000 ) ) ;
#7789=EDGE_CURVE ( 'NONE', #20876, #15884, #1425, .T. ) ;
#7813=CARTESIAN_POINT ( 'NONE',  ( -10.90000000000000036, 10.50000000000000000, 1.712914282636999961E-09 ) ) ;
#7833=CARTESIAN_POINT ( 'NONE',  ( -10.90000000000000036, 1.358133300253999998E-14, 0.000000000000000000 ) ) ;
#7836=DIRECTION ( 'NONE',  ( -1.000000000000000000, 0.000000000000000000, 0.000000000000000000 ) ) ;
#7893=EDGE_CURVE ( 'NONE', #14317, #3183, #6826, .T. ) ;
#7965=DIRECTION ( 'NONE',  ( 6.904857654351749962E-20, 1.420096922000000058E-10, -1.000000000000000000 ) ) ;
#7974=EDGE_LOOP ( 'NONE', ( #7436, #10656, #21169, #3242 ) ) ;
#7981=AXIS2_PLACEMENT_3D ( 'NONE', #17927, #23112, #2912 ) ;
#8034=APPLICATION_CONTEXT ( 'automotive_design' ) ;
#8080=ADVANCED_FACE ( 'NONE', ( #19160 ), #13780, .T. ) ;
#8182=DIRECTION ( 'NONE',  ( 6.905631305162550971E-20, -1.420100391446999833E-10, 1.000000000000000000 ) ) ;
#8234=EDGE_LOOP ( 'NONE', ( #14468, #8922, #19583, #10135 ) ) ;
#8264=DIRECTION ( 'NONE',  ( -1.000000000000000000, 0.000000000000000000, 0.000000000000000000 ) ) ;
#8340=DIRECTION ( 'NONE',  ( -1.000000000000000000, 0.000000000000000000, 0.000000000000000000 ) ) ;
#8542=EDGE_CURVE ( 'NONE', #7505, #6250, #16171, .T. ) ;
#8721=DIRECTION ( 'NONE',  ( -0.8206518066482797469, 0.5714285714285857187, 0.000000000000000000 ) ) ;
#8754=EDGE_CURVE ( 'NONE', #15925, #16101, #23772, .T. ) ;
#8805=VERTEX_POINT ( 'NONE', #14205 ) ;
#8813=CIRCLE ( 'NONE', #14213, 9.574826156038998448 ) ;
#8922=ORIENTED_EDGE ( 'NONE', *, *, #7730, .T. ) ;
#8958=EDGE_CURVE ( 'NONE', #14317, #568, #6374, .T. ) ;
#8983=CARTESIAN_POINT ( 'NONE',  ( 0.000000000000000000, 0.000000000000000000, 0.000000000000000000 ) ) ;
#9001=ORIENTED_EDGE ( 'NONE', *, *, #12487, .F. ) ;
#9037=SHAPE_DEFINITION_REPRESENTATION ( #18671, #14475 ) ;
#9053=MANIFOLD_SOLID_BREP ( 'Stock-MAS-673-1', #10020 ) ;
#9085=AXIS2_PLACEMENT_3D ( 'NONE', #13738, #8182, #10954 ) ;
#9111=PRESENTATION_STYLE_ASSIGNMENT (( #1721 ) ) ;
#9397=CARTESIAN_POINT ( 'NONE',  ( -8.099999999999999645, 1.323843189878000027E-14, 0.000000000000000000 ) ) ;
#9398=CARTESIAN_POINT ( 'NONE',  ( -10.25814758309999952, 1.350272875175999940E-14, 0.000000000000000000 ) ) ;
#9499=VECTOR ( 'NONE', #4540, 1000.000000000000000 ) ;
#9524=CIRCLE ( 'NONE', #21131, 10.50000000000000000 ) ;
#9551=AXIS2_PLACEMENT_3D ( 'NONE', #13301, #17061, #20700 ) ;
#9579=EDGE_LOOP ( 'NONE', ( #7602, #4194, #23764, #17067 ) ) ;
#9603=CIRCLE ( 'NONE', #11547, 10.50000000000000000 ) ;
#9617=AXIS2_PLACEMENT_3D ( 'NONE', #5368, #3327, #23656 ) ;
#9622=CARTESIAN_POINT ( 'NONE',  ( -11.00000000000000000, -10.50000000000000000, 0.000000000000000000 ) ) ;
#9623=CIRCLE ( 'NONE', #18906, 7.100000000000000533 ) ;
#9697=EDGE_CURVE ( 'NONE', #7168, #14405, #9623, .T. ) ;
#9803=ORIENTED_EDGE ( 'NONE', *, *, #7098, .T. ) ;
#9854=LINE ( 'NONE', #17484, #11068 ) ;
#9902=ORIENTED_EDGE ( 'NONE', *, *, #8542, .T. ) ;
#10004=CIRCLE ( 'NONE', #1509, 10.59999999999999964 ) ;
#10020=CLOSED_SHELL ( 'NONE', ( #21375, #821, #6885, #12658, #23145, #5970, #3170, #3131, #10316, #13959, #3015, #8080, #17060, #15443, #237, #303, #16333, #19350 ) ) ;
#10108=CARTESIAN_POINT ( 'NONE',  ( -10.90000000000000036, 7.100000000000000533, 1.377912020595000118E-10 ) ) ;
#10135=ORIENTED_EDGE ( 'NONE', *, *, #13260, .F. ) ;
#10206=DIRECTION ( 'NONE',  ( 0.000000000000000000, 0.9998843904358519774, 0.01520545174352925036 ) ) ;
#10210=AXIS2_PLACEMENT_3D ( 'NONE', #23204, #2997, #4936 ) ;
#10234=EDGE_CURVE ( 'NONE', #7505, #7147, #4261, .T. ) ;
#10316=ADVANCED_FACE ( 'NONE', ( #1435 ), #16606, .T. ) ;
#10511=DIRECTION ( 'NONE',  ( -6.780994087986969163E-22, -1.631350558111999873E-10, 1.000000000000000000 ) ) ;
#10556=DIRECTION ( 'NONE',  ( -1.734723475976817507E-14, 1.000000000000000000, 1.792956356300015483E-10 ) ) ;
#10561=AXIS2_PLACEMENT_3D ( 'NONE', #12141, #8264, #15511 ) ;
#10611=ORIENTED_EDGE ( 'NONE', *, *, #66, .F. ) ;
#10656=ORIENTED_EDGE ( 'NONE', *, *, #13260, .T. ) ;
#10710=AXIS2_PLACEMENT_3D ( 'NONE', #14390, #8340, #13906 ) ;
#10740=TOROIDAL_SURFACE ( 'NONE', #13813, 9.651424765286998664, 0.1000000000000000056 ) ;
#10776=CIRCLE ( 'NONE', #6508, 0.1000000000000002554 ) ;
#10820=DIRECTION ( 'NONE',  ( -1.000000000000000000, 0.000000000000000000, 0.000000000000000000 ) ) ;
#10852=DIRECTION ( 'NONE',  ( -5.739718509874449091E-40, -1.792960224733999962E-10, 1.000000000000000000 ) ) ;
#10932=SURFACE_STYLE_FILL_AREA ( #3548 ) ;
#10936=DIRECTION ( 'NONE',  ( -1.000000000000000000, 0.000000000000000000, 0.000000000000000000 ) ) ;
#10954=DIRECTION ( 'NONE',  ( 1.000000000000000000, 4.862776847858214598E-10, 0.000000000000000000 ) ) ;
#11008=PLANE ( 'NONE',  #3682 ) ;
#11021=EDGE_LOOP ( 'NONE', ( #17030, #16528, #20835, #716 ) ) ;
#11068=VECTOR ( 'NONE', #2582, 1000.000000000000000 ) ;
#11361=CARTESIAN_POINT ( 'NONE',  ( -8.035714285714000482, 1.323055916935999825E-14, 0.000000000000000000 ) ) ;
#11369=FACE_BOUND ( 'NONE', #1266, .T. ) ;
#11387=DIRECTION ( 'NONE',  ( 0.000000000000000000, 0.000000000000000000, 1.000000000000000000 ) ) ;
#11547=AXIS2_PLACEMENT_3D ( 'NONE', #16373, #10936, #18214 ) ;
#11589=CIRCLE ( 'NONE', #12384, 7.142857142857000241 ) ;
#11652=DIRECTION ( 'NONE',  ( -1.000000000000000000, 0.000000000000000000, 0.000000000000000000 ) ) ;
#11720=DIRECTION ( 'NONE',  ( -1.576598371538795140E-18, -7.363899292998020299E-10, 1.000000000000000000 ) ) ;
#11766=DIRECTION ( 'NONE',  ( 0.000000000000000000, 0.9998336578527885488, 0.01823887673933978840 ) ) ;
#11899=CIRCLE ( 'NONE', #23496, 10.59999999999999964 ) ;
#11920=DIRECTION ( 'NONE',  ( 0.000000000000000000, 1.000000000000000000, 0.000000000000000000 ) ) ;
#12082=DIRECTION ( 'NONE',  ( 0.000000000000000000, 1.000000000000000000, 0.000000000000000000 ) ) ;
#12098=CIRCLE ( 'NONE', #10561, 7.100000000000000533 ) ;
#12141=CARTESIAN_POINT ( 'NONE',  ( -10.34021276376999943, 1.351277883783999990E-14, 0.000000000000000000 ) ) ;
#12169=CARTESIAN_POINT ( 'NONE',  ( -10.90000000000000036, 1.358133300253999998E-14, 0.000000000000000000 ) ) ;
#12297=CARTESIAN_POINT ( 'NONE',  ( -10.90000000000000036, 7.100000000000000533, 0.000000000000000000 ) ) ;
#12311=CARTESIAN_POINT ( 'NONE',  ( -10.34021276376999943, 1.351277883783999990E-14, 0.000000000000000000 ) ) ;
#12332=AXIS2_PLACEMENT_3D ( 'NONE', #21699, #6912, #10556 ) ;
#12350=CIRCLE ( 'NONE', #9617, 12.50000000000000533 ) ;
#12358=ORIENTED_EDGE ( 'NONE', *, *, #19645, .T. ) ;
#12361=DIRECTION ( 'NONE',  ( 0.000000000000000000, 0.000000000000000000, -1.000000000000000000 ) ) ;
#12384=AXIS2_PLACEMENT_3D ( 'NONE', #9398, #3598, #16661 ) ;
#12391=CARTESIAN_POINT ( 'NONE',  ( -8.000000000000000000, -9.651424765286998664, 0.000000000000000000 ) ) ;
#12392=FACE_OUTER_BOUND ( 'NONE', #11021, .T. ) ;
#12487=EDGE_CURVE ( 'NONE', #568, #14317, #9603, .T. ) ;
#12535=CARTESIAN_POINT ( 'NONE',  ( -10.90000000000000036, -10.59999999999999964, 0.000000000000000000 ) ) ;
#12547=CARTESIAN_POINT ( 'NONE',  ( 0.5500000000000000444, 1.217911241751999838E-14, 0.000000000000000000 ) ) ;
#12658=ADVANCED_FACE ( 'NONE', ( #13570 ), #2548, .F. ) ;
#12684=FACE_OUTER_BOUND ( 'NONE', #13869, .T. ) ;
#12701=ORIENTED_EDGE ( 'NONE', *, *, #20043, .F. ) ;
#12720=CIRCLE ( 'NONE', #18498, 9.651424765286998664 ) ;
#12749=AXIS2_PLACEMENT_3D ( 'NONE', #3146, #19845, #11766 ) ;
#12762=ORIENTED_EDGE ( 'NONE', *, *, #143, .T. ) ;
#12772=EDGE_CURVE ( 'NONE', #6250, #3348, #15396, .T. ) ;
#12788=ORIENTED_EDGE ( 'NONE', *, *, #13076, .T. ) ;
#12798=EDGE_CURVE ( 'NONE', #7168, #16445, #10776, .T. ) ;
#12820=EDGE_CURVE ( 'NONE', #7147, #3183, #2248, .T. ) ;
#12988=ORIENTED_EDGE ( 'NONE', *, *, #12772, .T. ) ;
#13033=CARTESIAN_POINT ( 'NONE',  ( -10.90000000000000036, 1.358133300253999998E-14, 0.000000000000000000 ) ) ;
#13076=EDGE_CURVE ( 'NONE', #6250, #7505, #10004, .T. ) ;
#13108=ORIENTED_EDGE ( 'NONE', *, *, #20912, .T. ) ;
#13194=DIRECTION ( 'NONE',  ( 0.000000000000000000, 0.9998172265789604385, 0.01911840568550923769 ) ) ;
#13260=EDGE_CURVE ( 'NONE', #14405, #7168, #18524, .T. ) ;
#13301=CARTESIAN_POINT ( 'NONE',  ( 0.000000000000000000, 1.224646799146999965E-14, 0.000000000000000000 ) ) ;
#13346=AXIS2_PLACEMENT_3D ( 'NONE', #811, #323, #7728 ) ;
#13530=EDGE_CURVE ( 'NONE', #8805, #16101, #12350, .T. ) ;
#13570=FACE_OUTER_BOUND ( 'NONE', #6607, .T. ) ;
#13597=DIRECTION ( 'NONE',  ( -1.000000000000000000, 0.000000000000000000, 0.000000000000000000 ) ) ;
#13673=ORIENTED_EDGE ( 'NONE', *, *, #13530, .F. ) ;
#13685=EDGE_CURVE ( 'NONE', #16101, #15884, #6853, .T. ) ;
#13738=CARTESIAN_POINT ( 'NONE',  ( -8.099999999999999645, -9.651424765286998664, -1.370599189697999991E-09 ) ) ;
#13754=ORIENTED_EDGE ( 'NONE', *, *, #21636, .T. ) ;
#13780=TOROIDAL_SURFACE ( 'NONE', #21904, 10.50000000000000000, 0.1000000000000000056 ) ;
#13813=AXIS2_PLACEMENT_3D ( 'NONE', #18528, #222, #18880 ) ;
#13851=PRODUCT ( 'Ball Seat Ring', 'Ball Seat Ring', '', ( #6855 ) ) ;
#13869=EDGE_LOOP ( 'NONE', ( #21272, #33, #6733, #1959 ) ) ;
#13906=DIRECTION ( 'NONE',  ( 0.000000000000000000, 0.9997423213046380264, 0.02270002185933085032 ) ) ;
#13959=ADVANCED_FACE ( 'NONE', ( #14881 ), #10740, .T. ) ;
#14096=CARTESIAN_POINT ( 'NONE',  ( -8.000000000000000000, 1.322618543078999814E-14, 0.000000000000000000 ) ) ;
#14202=FACE_OUTER_BOUND ( 'NONE', #18966, .T. ) ;
#14205=CARTESIAN_POINT ( 'NONE',  ( -10.25814758309999952, -7.142857142857000241, 0.000000000000000000 ) ) ;
#14213=AXIS2_PLACEMENT_3D ( 'NONE', #11361, #7836, #5892 ) ;
#14317=VERTEX_POINT ( 'NONE', #18619 ) ;
#14390=CARTESIAN_POINT ( 'NONE',  ( -10.90000000000000036, 1.358133300253999998E-14, 0.000000000000000000 ) ) ;
#14405=VERTEX_POINT ( 'NONE', #3966 ) ;
#14463=AXIS2_PLACEMENT_3D ( 'NONE', #3241, #21522, #12082 ) ;
#14468=ORIENTED_EDGE ( 'NONE', *, *, #19568, .T. ) ;
#14475=SHAPE_REPRESENTATION ( 'Ball Seat Ring', ( #4390 ), #20254 ) ;
#14581=AXIS2_PLACEMENT_3D ( 'NONE', #4109, #18649, #11387 ) ;
#14641=TOROIDAL_SURFACE ( 'NONE', #16956, 10.50000000000000000, 0.1000000000000000056 ) ;
#14649=EDGE_LOOP ( 'NONE', ( #12762, #17277, #352, #9001 ) ) ;
#14679=ORIENTED_EDGE ( 'NONE', *, *, #21636, .F. ) ;
#14764=DIRECTION ( 'NONE',  ( 0.000000000000000000, 0.000000000000000000, -1.000000000000000000 ) ) ;
#14881=FACE_OUTER_BOUND ( 'NONE', #9579, .T. ) ;
#14975=TOROIDAL_SURFACE ( 'NONE', #2619, 7.200000000000000178, 0.1000000000000000056 ) ;
#14997=AXIS2_PLACEMENT_3D ( 'NONE', #22765, #21205, #19640 ) ;
#15204=DIRECTION ( 'NONE',  ( -1.000000000000000000, 0.000000000000000000, 0.000000000000000000 ) ) ;
#15263=VERTEX_POINT ( 'NONE', #23062 ) ;
#15396=CIRCLE ( 'NONE', #12332, 0.09999999999999939493 ) ;
#15422=LINE ( 'NONE', #10108, #831 ) ;
#15440=VECTOR ( 'NONE', #370, 1000.000000000000000 ) ;
#15443=ADVANCED_FACE ( 'NONE', ( #1755 ), #20284, .T. ) ;
#15450=CARTESIAN_POINT ( 'NONE',  ( -10.25814758309999952, 1.350272875175999940E-14, 0.000000000000000000 ) ) ;
#15455=EDGE_CURVE ( 'NONE', #20876, #15263, #2973, .T. ) ;
#15458=EDGE_CURVE ( 'NONE', #7505, #20171, #23069, .T. ) ;
#15511=DIRECTION ( 'NONE',  ( 0.000000000000000000, 1.000000000000000000, 0.000000000000000000 ) ) ;
#15532=DIRECTION ( 'NONE',  ( -1.000000000000000000, 0.000000000000000000, 0.000000000000000000 ) ) ;
#15677=AXIS2_PLACEMENT_3D ( 'NONE', #18183, #20112, #23246 ) ;
#15703=DIRECTION ( 'NONE',  ( 0.000000000000000000, 1.000000000000000000, 0.000000000000000000 ) ) ;
#15833=CARTESIAN_POINT ( 'NONE',  ( -8.099999999999999645, 1.323843189878000027E-14, 0.000000000000000000 ) ) ;
#15884=VERTEX_POINT ( 'NONE', #19528 ) ;
#15925=VERTEX_POINT ( 'NONE', #12391 ) ;
#15945=FACE_OUTER_BOUND ( 'NONE', #7974, .T. ) ;
#15955=CARTESIAN_POINT ( 'NONE',  ( -8.035714285714000482, -9.574826156038998448, 0.000000000000000000 ) ) ;
#15975=PRODUCT_DEFINITION_FORMATION_WITH_SPECIFIED_SOURCE ( 'ANY', '', #13851, .NOT_KNOWN. ) ;
#16101=VERTEX_POINT ( 'NONE', #15955 ) ;
#16113=EDGE_CURVE ( 'NONE', #15925, #21756, #12720, .T. ) ;
#16135=AXIS2_PLACEMENT_3D ( 'NONE', #20794, #10511, #5175 ) ;
#16171=CIRCLE ( 'NONE', #1868, 10.59999999999999964 ) ;
#16183=AXIS2_PLACEMENT_3D ( 'NONE', #13033, #13597, #16668 ) ;
#16207=FACE_OUTER_BOUND ( 'NONE', #14649, .T. ) ;
#16333=ADVANCED_FACE ( 'NONE', ( #16207 ), #14641, .T. ) ;
#16346=CARTESIAN_POINT ( 'NONE',  ( -10.90000000000000036, 1.358133300253999998E-14, 0.000000000000000000 ) ) ;
#16373=CARTESIAN_POINT ( 'NONE',  ( -11.00000000000000000, 1.359357947053999856E-14, 0.000000000000000000 ) ) ;
#16445=VERTEX_POINT ( 'NONE', #17620 ) ;
#16521=DIRECTION ( 'NONE',  ( 0.000000000000000000, 1.000000000000000000, 0.000000000000000000 ) ) ;
#16528=ORIENTED_EDGE ( 'NONE', *, *, #22945, .T. ) ;
#16537=DIRECTION ( 'NONE',  ( -1.000000000000000000, 0.000000000000000000, 0.000000000000000000 ) ) ;
#16557=EDGE_LOOP ( 'NONE', ( #13108, #18734 ) ) ;
#16586=SPHERICAL_SURFACE ( 'NONE', #2996, 12.50000000000000000 ) ;
#16588=( NAMED_UNIT ( * ) SI_UNIT ( $, .STERADIAN. ) SOLID_ANGLE_UNIT ( ) );
#16606=TOROIDAL_SURFACE ( 'NONE', #12749, 9.651424765286998664, 0.1000000000000000056 ) ;
#16631=AXIS2_PLACEMENT_3D ( 'NONE', #22248, #11720, #19095 ) ;
#16661=DIRECTION ( 'NONE',  ( 0.000000000000000000, 1.000000000000000000, 0.000000000000000000 ) ) ;
#16668=DIRECTION ( 'NONE',  ( 0.000000000000000000, -1.000000000000000000, 0.000000000000000000 ) ) ;
#16696=ORIENTED_EDGE ( 'NONE', *, *, #15458, .F. ) ;
#16765=DIRECTION ( 'NONE',  ( -6.752000474851949799E-22, 1.631346932539999964E-10, -1.000000000000000000 ) ) ;
#16801=CARTESIAN_POINT ( 'NONE',  ( -8.099999999999999645, 10.59999999999999964, 0.000000000000000000 ) ) ;
#16808=ORIENTED_EDGE ( 'NONE', *, *, #10234, .T. ) ;
#16954=AXIS2_PLACEMENT_3D ( 'NONE', #21541, #4956, #19483 ) ;
#16956=AXIS2_PLACEMENT_3D ( 'NONE', #21788, #5203, #525 ) ;
#17030=ORIENTED_EDGE ( 'NONE', *, *, #15455, .T. ) ;
#17060=ADVANCED_FACE ( 'NONE', ( #12684 ), #3462, .T. ) ;
#17061=DIRECTION ( 'NONE',  ( 0.000000000000000000, 0.000000000000000000, -1.000000000000000000 ) ) ;
#17067=ORIENTED_EDGE ( 'NONE', *, *, #16113, .F. ) ;
#17277=ORIENTED_EDGE ( 'NONE', *, *, #12820, .T. ) ;
#17286=DIRECTION ( 'NONE',  ( 1.000000000000000000, -4.862256430815421556E-10, 0.000000000000000000 ) ) ;
#17348=CARTESIAN_POINT ( 'NONE',  ( -8.099999999999999645, 1.323843189878000027E-14, 0.000000000000000000 ) ) ;
#17408=ORIENTED_EDGE ( 'NONE', *, *, #7098, .F. ) ;
#17484=CARTESIAN_POINT ( 'NONE',  ( -10.90000000000000036, -7.100000000000000533, -1.377928257607000217E-10 ) ) ;
#17499=TOROIDAL_SURFACE ( 'NONE', #22143, 7.200000000000000178, 0.1000000000000000056 ) ;
#17510=EDGE_LOOP ( 'NONE', ( #13673, #18934, #20414, #5935 ) ) ;
#17544=DIRECTION ( 'NONE',  ( -1.000000000000000000, 0.000000000000000000, 0.000000000000000000 ) ) ;
#17618=DIRECTION ( 'NONE',  ( 0.000000000000000000, -1.000000000000000000, 0.000000000000000000 ) ) ;
#17620=CARTESIAN_POINT ( 'NONE',  ( -11.00000000000000000, 7.200000000000000178, 0.000000000000000000 ) ) ;
#17681=DIRECTION ( 'NONE',  ( -1.000000000000000000, 0.000000000000000000, 0.000000000000000000 ) ) ;
#17794=CYLINDRICAL_SURFACE ( 'NONE', #16954, 7.100000000000000533 ) ;
#17809=EDGE_CURVE ( 'NONE', #20876, #8805, #11589, .T. ) ;
#17927=CARTESIAN_POINT ( 'NONE',  ( -11.00000000000000000, 1.359357947053999856E-14, 0.000000000000000000 ) ) ;
#17932=DIRECTION ( 'NONE',  ( -1.000000000000000000, 0.000000000000000000, 0.000000000000000000 ) ) ;
#18028=CIRCLE ( 'NONE', #13346, 0.1000000000000002554 ) ;
#18063=AXIS2_PLACEMENT_3D ( 'NONE', #7813, #16765, #18952 ) ;
#18070=AXIS2_PLACEMENT_3D ( 'NONE', #6968, #20051, #3467 ) ;
#18085=CARTESIAN_POINT ( 'NONE',  ( -10.34021276376999943, 1.351277883783999990E-14, 0.000000000000000000 ) ) ;
#18088=DIRECTION ( 'NONE',  ( 0.000000000000000000, 1.000000000000000000, 0.000000000000000000 ) ) ;
#18089=ORIENTED_EDGE ( 'NONE', *, *, #7730, .F. ) ;
#18093=ORIENTED_EDGE ( 'NONE', *, *, #12820, .F. ) ;
#18122=CARTESIAN_POINT ( 'NONE',  ( -8.099999999999999645, -10.50000000000000000, -1.882608235970000037E-09 ) ) ;
#18183=CARTESIAN_POINT ( 'NONE',  ( -11.00000000000000000, 1.359357947053999856E-14, 0.000000000000000000 ) ) ;
#18214=DIRECTION ( 'NONE',  ( 0.000000000000000000, -1.000000000000000000, 0.000000000000000000 ) ) ;
#18215=EDGE_LOOP ( 'NONE', ( #12988, #13754, #16696, #7611 ) ) ;
#18224=ORIENTED_EDGE ( 'NONE', *, *, #8958, .T. ) ;
#18234=DIRECTION ( 'NONE',  ( -1.734723475976817507E-14, -1.000000000000000000, -1.792960224734025295E-10 ) ) ;
#18318=SURFACE_SIDE_STYLE ('',( #10932 ) ) ;
#18356=ORIENTED_EDGE ( 'NONE', *, *, #9697, .F. ) ;
#18364=COLOUR_RGB ( '', 0.40784314, 0.44705882, 0.49803922) ;
#18403=DIRECTION ( 'NONE',  ( 0.000000000000000000, 5.996561511235000638E-10, -1.000000000000000000 ) ) ;
#18439=AXIS2_PLACEMENT_3D ( 'NONE', #18122, #10852, #18234 ) ;
#18480=CARTESIAN_POINT ( 'NONE',  ( -8.099999999999999645, 1.323843189878000027E-14, 0.000000000000000000 ) ) ;
#18498=AXIS2_PLACEMENT_3D ( 'NONE', #2783, #23103, #6529 ) ;
#18503=AXIS2_PLACEMENT_3D ( 'NONE', #16346, #23734, #5336 ) ;
#18524=CIRCLE ( 'NONE', #16183, 7.100000000000000533 ) ;
#18528=CARTESIAN_POINT ( 'NONE',  ( -8.099999999999999645, 1.323843189878000027E-14, 0.000000000000000000 ) ) ;
#18530=SPHERICAL_SURFACE ( 'NONE', #9551, 12.50000000000000000 ) ;
#18538=CARTESIAN_POINT ( 'NONE',  ( -10.34021276376999943, 1.351277883783999990E-14, 0.000000000000000000 ) ) ;
#18583=ORIENTED_EDGE ( 'NONE', *, *, #7789, .F. ) ;
#18619=CARTESIAN_POINT ( 'NONE',  ( -11.00000000000000000, 10.50000000000000000, 0.000000000000000000 ) ) ;
#18630=CARTESIAN_POINT ( 'NONE',  ( -11.00000000000000000, 1.359357947053999856E-14, 0.000000000000000000 ) ) ;
#18649=DIRECTION ( 'NONE',  ( -1.000000000000000000, 0.000000000000000000, 0.000000000000000000 ) ) ;
#18671=PRODUCT_DEFINITION_SHAPE ( 'NONE', 'NONE',  #116 ) ;
#18672=DIRECTION ( 'NONE',  ( 0.000000000000000000, 1.000000000000000000, 0.000000000000000000 ) ) ;
#18734=ORIENTED_EDGE ( 'NONE', *, *, #16113, .T. ) ;
#18800=AXIS2_PLACEMENT_3D ( 'NONE', #12311, #23310, #1641 ) ;
#18880=DIRECTION ( 'NONE',  ( 0.000000000000000000, -0.9998336578527885488, -0.01823887673933978840 ) ) ;
#18906=AXIS2_PLACEMENT_3D ( 'NONE', #2910, #17681, #21681 ) ;
#18934=ORIENTED_EDGE ( 'NONE', *, *, #79, .T. ) ;
#18952=DIRECTION ( 'NONE',  ( -1.000000000000000000, -4.145989107584593997E-12, 0.000000000000000000 ) ) ;
#18966=EDGE_LOOP ( 'NONE', ( #23920, #21516, #4103, #22781 ) ) ;
#19012=( NAMED_UNIT ( * ) PLANE_ANGLE_UNIT ( ) SI_UNIT ( $, .RADIAN. ) );
#19095=DIRECTION ( 'NONE',  ( 0.8206518289197470839, 0.5714285394436248167, 4.207942230546201995E-10 ) ) ;
#19153=ORIENTED_EDGE ( 'NONE', *, *, #8754, .F. ) ;
#19160=FACE_OUTER_BOUND ( 'NONE', #18215, .T. ) ;
#19187=LINE ( 'NONE', #22931, #9499 ) ;
#19226=ORIENTED_EDGE ( 'NONE', *, *, #13530, .T. ) ;
#19235=ORIENTED_EDGE ( 'NONE', *, *, #20043, .T. ) ;
#19350=ADVANCED_FACE ( 'NONE', ( #11369, #1803 ), #11008, .T. ) ;
#19483=DIRECTION ( 'NONE',  ( 0.000000000000000000, 1.000000000000000000, 0.000000000000000000 ) ) ;
#19503=CARTESIAN_POINT ( 'NONE',  ( -11.00000000000000000, -7.200000000000000178, 0.000000000000000000 ) ) ;
#19528=CARTESIAN_POINT ( 'NONE',  ( -8.035714285714000482, 9.574826156038998448, 0.000000000000000000 ) ) ;
#19537=STYLED_ITEM ( 'NONE', ( #9111 ), #9053 ) ;
#19553=CARTESIAN_POINT ( 'NONE',  ( -8.000000000000000000, 1.322618543078999814E-14, 0.000000000000000000 ) ) ;
#19559=DIRECTION ( 'NONE',  ( -1.000000000000000000, 0.000000000000000000, 0.000000000000000000 ) ) ;
#19568=EDGE_CURVE ( 'NONE', #14405, #7738, #18028, .T. ) ;
#19583=ORIENTED_EDGE ( 'NONE', *, *, #12798, .F. ) ;
#19640=DIRECTION ( 'NONE',  ( 0.000000000000000000, 1.000000000000000000, 0.000000000000000000 ) ) ;
#19645=EDGE_CURVE ( 'NONE', #21756, #15884, #20703, .T. ) ;
#19825=ORIENTED_EDGE ( 'NONE', *, *, #678, .F. ) ;
#19845=DIRECTION ( 'NONE',  ( -1.000000000000000000, 0.000000000000000000, 0.000000000000000000 ) ) ;
#20001=AXIS2_PLACEMENT_3D ( 'NONE', #12547, #23560, #16521 ) ;
#20043=EDGE_CURVE ( 'NONE', #16445, #7738, #2151, .T. ) ;
#20051=DIRECTION ( 'NONE',  ( 1.576486815247195039E-18, 7.363894760761759519E-10, -1.000000000000000000 ) ) ;
#20112=DIRECTION ( 'NONE',  ( -1.000000000000000000, 0.000000000000000000, 0.000000000000000000 ) ) ;
#20140=FILL_AREA_STYLE_COLOUR ( '', #18364 ) ;
#20171=VERTEX_POINT ( 'NONE', #7484 ) ;
#20239=( LENGTH_UNIT ( ) NAMED_UNIT ( * ) SI_UNIT ( .MILLI., .METRE. ) );
#20242=DIRECTION ( 'NONE',  ( -1.000000000000000000, 0.000000000000000000, 0.000000000000000000 ) ) ;
#20254=( GEOMETRIC_REPRESENTATION_CONTEXT ( 3 ) GLOBAL_UNCERTAINTY_ASSIGNED_CONTEXT ( ( #1677 ) ) GLOBAL_UNIT_ASSIGNED_CONTEXT ( ( #20239, #7384, #16588 ) ) REPRESENTATION_CONTEXT ( 'NONE', 'WORKASPACE' ) );
#20284=CYLINDRICAL_SURFACE ( 'NONE', #20001, 10.59999999999999964 ) ;
#20350=DIRECTION ( 'NONE',  ( 0.000000000000000000, 1.000000000000000000, 0.000000000000000000 ) ) ;
#20373=EDGE_CURVE ( 'NONE', #1761, #15263, #2547, .T. ) ;
#20414=ORIENTED_EDGE ( 'NONE', *, *, #7789, .T. ) ;
#20471=FACE_BOUND ( 'NONE', #16557, .T. ) ;
#20620=EDGE_CURVE ( 'NONE', #14405, #1761, #9854, .T. ) ;
#20700=DIRECTION ( 'NONE',  ( 0.000000000000000000, 1.000000000000000000, 0.000000000000000000 ) ) ;
#20703=CIRCLE ( 'NONE', #6792, 0.09999999999999939493 ) ;
#20787=AXIS2_PLACEMENT_3D ( 'NONE', #5715, #11652, #7771 ) ;
#20794=CARTESIAN_POINT ( 'NONE',  ( -10.90000000000000036, -10.50000000000000000, -1.712918112906000235E-09 ) ) ;
#20804=CARTESIAN_POINT ( 'NONE',  ( -8.099999999999999645, 9.651424765286998664, 1.370595831274000043E-09 ) ) ;
#20835=ORIENTED_EDGE ( 'NONE', *, *, #1992, .F. ) ;
#20873=TOROIDAL_SURFACE ( 'NONE', #1155, 7.200000000000000178, 0.1000000000000000056 ) ;
#20876=VERTEX_POINT ( 'NONE', #7768 ) ;
#20912=EDGE_CURVE ( 'NONE', #21756, #15925, #1424, .T. ) ;
#21076=AXIS2_PLACEMENT_3D ( 'NONE', #7399, #23760, #18088 ) ;
#21131=AXIS2_PLACEMENT_3D ( 'NONE', #14096, #19559, #17618 ) ;
#21169=ORIENTED_EDGE ( 'NONE', *, *, #4994, .T. ) ;
#21205=DIRECTION ( 'NONE',  ( -1.000000000000000000, 0.000000000000000000, 0.000000000000000000 ) ) ;
#21272=ORIENTED_EDGE ( 'NONE', *, *, #15458, .T. ) ;
#21375=ADVANCED_FACE ( 'NONE', ( #23598 ), #240, .T. ) ;
#21388=ORIENTED_EDGE ( 'NONE', *, *, #7893, .T. ) ;
#21434=CARTESIAN_POINT ( 'NONE',  ( -10.34021276376999943, -7.100000000000000533, 0.000000000000000000 ) ) ;
#21516=ORIENTED_EDGE ( 'NONE', *, *, #20373, .T. ) ;
#21522=DIRECTION ( 'NONE',  ( -1.000000000000000000, 0.000000000000000000, 0.000000000000000000 ) ) ;
#21541=CARTESIAN_POINT ( 'NONE',  ( 0.5500000000000000444, 1.217911241751999838E-14, 0.000000000000000000 ) ) ;
#21561=CARTESIAN_POINT ( 'NONE',  ( 0.000000000000000000, 0.000000000000000000, 0.000000000000000000 ) ) ;
#21636=EDGE_CURVE ( 'NONE', #3348, #20171, #22679, .T. ) ;
#21681=DIRECTION ( 'NONE',  ( 0.000000000000000000, 1.000000000000000000, 0.000000000000000000 ) ) ;
#21699=CARTESIAN_POINT ( 'NONE',  ( -8.099999999999999645, 10.50000000000000000, 1.882604183655999859E-09 ) ) ;
#21756=VERTEX_POINT ( 'NONE', #489 ) ;
#21762=FACE_OUTER_BOUND ( 'NONE', #22950, .T. ) ;
#21788=CARTESIAN_POINT ( 'NONE',  ( -10.90000000000000036, 1.358133300253999998E-14, 0.000000000000000000 ) ) ;
#21904=AXIS2_PLACEMENT_3D ( 'NONE', #17348, #2704, #10206 ) ;
#22110=APPLICATION_CONTEXT ( 'automotive_design' ) ;
#22143=AXIS2_PLACEMENT_3D ( 'NONE', #18538, #20242, #13194 ) ;
#22183=CARTESIAN_POINT ( 'NONE',  ( -8.099999999999999645, -10.59999999999999964, -4.735481798356999505E-10 ) ) ;
#22224=( GEOMETRIC_REPRESENTATION_CONTEXT ( 3 ) GLOBAL_UNCERTAINTY_ASSIGNED_CONTEXT ( ( #23717 ) ) GLOBAL_UNIT_ASSIGNED_CONTEXT ( ( #1957, #19012, #595 ) ) REPRESENTATION_CONTEXT ( 'NONE', 'WORKASPACE' ) );
#22248=CARTESIAN_POINT ( 'NONE',  ( -10.34021276376999943, -7.200000000000000178, -5.302007471952000326E-09 ) ) ;
#22272=FACE_OUTER_BOUND ( 'NONE', #5025, .T. ) ;
#22421=DIRECTION ( 'NONE',  ( -1.000000000000000000, 0.000000000000000000, 0.000000000000000000 ) ) ;
#22601=DIRECTION ( 'NONE',  ( 0.000000000000000000, -1.000000000000000000, 0.000000000000000000 ) ) ;
#22666=CIRCLE ( 'NONE', #7981, 7.200000000000000178 ) ;
#22679=CIRCLE ( 'NONE', #23076, 10.50000000000000000 ) ;
#22765=CARTESIAN_POINT ( 'NONE',  ( 0.5500000000000000444, 1.217911241751999838E-14, 0.000000000000000000 ) ) ;
#22781=ORIENTED_EDGE ( 'NONE', *, *, #79, .F. ) ;
#22809=DIRECTION ( 'NONE',  ( 1.000000000000000000, 0.000000000000000000, 2.088600023070000287E-09 ) ) ;
#22830=ORIENTED_EDGE ( 'NONE', *, *, #10234, .F. ) ;
#22836=DIRECTION ( 'NONE',  ( -1.000000000000000000, 0.000000000000000000, 0.000000000000000000 ) ) ;
#22931=CARTESIAN_POINT ( 'NONE',  ( -8.099999999999999645, 10.59999999999999964, 4.735458969396000849E-10 ) ) ;
#22941=ORIENTED_EDGE ( 'NONE', *, *, #12487, .T. ) ;
#22945=EDGE_CURVE ( 'NONE', #15263, #1761, #12098, .T. ) ;
#22950=EDGE_LOOP ( 'NONE', ( #21388, #6705, #1829, #1728 ) ) ;
#23045=DIRECTION ( 'NONE',  ( -1.000000000000000000, 0.000000000000000000, 0.000000000000000000 ) ) ;
#23062=CARTESIAN_POINT ( 'NONE',  ( -10.34021276376999943, 7.100000000000000533, 0.000000000000000000 ) ) ;
#23069=CIRCLE ( 'NONE', #18439, 0.09999999999999939493 ) ;
#23073=CYLINDRICAL_SURFACE ( 'NONE', #14463, 10.59999999999999964 ) ;
#23076=AXIS2_PLACEMENT_3D ( 'NONE', #19553, #15532, #11920 ) ;
#23100=CARTESIAN_POINT ( 'NONE',  ( -10.90000000000000036, 10.59999999999999964, 0.000000000000000000 ) ) ;
#23103=DIRECTION ( 'NONE',  ( -1.000000000000000000, 0.000000000000000000, 0.000000000000000000 ) ) ;
#23112=DIRECTION ( 'NONE',  ( -1.000000000000000000, 0.000000000000000000, 0.000000000000000000 ) ) ;
#23145=ADVANCED_FACE ( 'NONE', ( #12392 ), #17499, .T. ) ;
#23204=CARTESIAN_POINT ( 'NONE',  ( -10.90000000000000036, 1.358133300253999998E-14, 0.000000000000000000 ) ) ;
#23246=DIRECTION ( 'NONE',  ( 0.000000000000000000, 1.000000000000000000, 0.000000000000000000 ) ) ;
#23310=DIRECTION ( 'NONE',  ( -1.000000000000000000, 0.000000000000000000, 0.000000000000000000 ) ) ;
#23496=AXIS2_PLACEMENT_3D ( 'NONE', #7833, #15204, #2497 ) ;
#23560=DIRECTION ( 'NONE',  ( -1.000000000000000000, 0.000000000000000000, 0.000000000000000000 ) ) ;
#23598=FACE_OUTER_BOUND ( 'NONE', #3229, .T. ) ;
#23656=DIRECTION ( 'NONE',  ( -0.8206518066482797469, -0.5714285714285857187, 0.000000000000000000 ) ) ;
#23669=PRODUCT_DEFINITION_CONTEXT ( 'detailed design', #22110, 'design' ) ;
#23717=UNCERTAINTY_MEASURE_WITH_UNIT (LENGTH_MEASURE( 1.000000000000000082E-05 ), #1957, 'distance_accuracy_value', 'NONE');
#23734=DIRECTION ( 'NONE',  ( -1.000000000000000000, 0.000000000000000000, 0.000000000000000000 ) ) ;
#23760=DIRECTION ( 'NONE',  ( -1.000000000000000000, 0.000000000000000000, 0.000000000000000000 ) ) ;
#23764=ORIENTED_EDGE ( 'NONE', *, *, #19645, .F. ) ;
#23772=CIRCLE ( 'NONE', #9085, 0.09999999999999939493 ) ;
#23856=DIRECTION ( 'NONE',  ( 0.000000000000000000, 0.000000000000000000, 1.000000000000000000 ) ) ;
#23920=ORIENTED_EDGE ( 'NONE', *, *, #1992, .T. ) ;
ENDSEC;
END-ISO-10303-21;
